ISO-10303-21;
HEADER;
/* Generated by software containing ST-Developer
 * from STEP Tools, Inc. (www.steptools.com) 
 */

FILE_DESCRIPTION(
/* description */ ('Indexing fixture plate with plunger'),
/* implementation_level */ '2;1');

FILE_NAME(
/* name */ 'Socket Set Screw - M5x8.step',
/* time_stamp */ '2026-10-28T03:23:41-07:00',
/* author */ (''),
/* organization */ (''),
/* preprocessor_version */ 'ST-DEVELOPER v20.2',
/* originating_system */ 'Autodesk Translation Framework v15.17.0.0',
/* authorisation */ '');

FILE_SCHEMA (('AUTOMOTIVE_DESIGN { 1 0 10303 214 3 1 1 }'));
ENDSEC;

DATA;
#10=MECHANICAL_DESIGN_GEOMETRIC_PRESENTATION_REPRESENTATION('',(#352),#10020);
#227=CONICAL_SURFACE('',#5560,0.235,0.785398163397448);
#228=CONICAL_SURFACE('',#5564,0.2125,0.785398163397448);
#289=SHAPE_REPRESENTATION_RELATIONSHIP('SRR','None',#10166,#316);
#316=ADVANCED_BREP_SHAPE_REPRESENTATION('',(#386),#10019);
#352=STYLED_ITEM('',(#10375),#386);
#386=MANIFOLD_SOLID_BREP('Body1',#4608);
#536=FACE_BOUND('',#1387,.T.);
#661=PLANE('',#5551);
#662=PLANE('',#5552);
#663=PLANE('',#5553);
#664=PLANE('',#5554);
#665=PLANE('',#5555);
#666=PLANE('',#5556);
#667=PLANE('',#5557);
#668=PLANE('',#5558);
#669=PLANE('',#5566);
#944=FACE_OUTER_BOUND('',#1379,.T.);
#945=FACE_OUTER_BOUND('',#1380,.T.);
#946=FACE_OUTER_BOUND('',#1381,.T.);
#947=FACE_OUTER_BOUND('',#1382,.T.);
#948=FACE_OUTER_BOUND('',#1383,.T.);
#949=FACE_OUTER_BOUND('',#1384,.T.);
#950=FACE_OUTER_BOUND('',#1385,.T.);
#951=FACE_OUTER_BOUND('',#1386,.T.);
#952=FACE_OUTER_BOUND('',#1388,.T.);
#953=FACE_OUTER_BOUND('',#1389,.T.);
#954=FACE_OUTER_BOUND('',#1390,.T.);
#955=FACE_OUTER_BOUND('',#1391,.T.);
#1379=EDGE_LOOP('',(#4117,#4118,#4119,#4120));
#1380=EDGE_LOOP('',(#4121,#4122,#4123,#4124));
#1381=EDGE_LOOP('',(#4125,#4126,#4127,#4128));
#1382=EDGE_LOOP('',(#4129,#4130,#4131,#4132));
#1383=EDGE_LOOP('',(#4133,#4134,#4135,#4136));
#1384=EDGE_LOOP('',(#4137,#4138,#4139,#4140));
#1385=EDGE_LOOP('',(#4141,#4142,#4143,#4144,#4145,#4146));
#1386=EDGE_LOOP('',(#4147));
#1387=EDGE_LOOP('',(#4148,#4149,#4150,#4151,#4152,#4153));
#1388=EDGE_LOOP('',(#4154,#4155,#4156,#4157));
#1389=EDGE_LOOP('',(#4158,#4159,#4160,#4161));
#1390=EDGE_LOOP('',(#4162,#4163,#4164,#4165));
#1391=EDGE_LOOP('',(#4166));
#1591=LINE('',#9899,#1811);
#1592=LINE('',#9901,#1812);
#1593=LINE('',#9903,#1813);
#1594=LINE('',#9904,#1814);
#1595=LINE('',#9907,#1815);
#1596=LINE('',#9909,#1816);
#1597=LINE('',#9910,#1817);
#1598=LINE('',#9913,#1818);
#1599=LINE('',#9915,#1819);
#1600=LINE('',#9916,#1820);
#1601=LINE('',#9919,#1821);
#1602=LINE('',#9921,#1822);
#1603=LINE('',#9922,#1823);
#1604=LINE('',#9925,#1824);
#1605=LINE('',#9927,#1825);
#1606=LINE('',#9928,#1826);
#1607=LINE('',#9930,#1827);
#1608=LINE('',#9931,#1828);
#1609=LINE('',#9939,#1829);
#1610=LINE('',#9943,#1830);
#1611=LINE('',#9947,#1831);
#1811=VECTOR('',#7062,1.);
#1812=VECTOR('',#7063,1.);
#1813=VECTOR('',#7064,1.);
#1814=VECTOR('',#7065,1.);
#1815=VECTOR('',#7068,1.);
#1816=VECTOR('',#7069,1.);
#1817=VECTOR('',#7070,1.);
#1818=VECTOR('',#7073,1.);
#1819=VECTOR('',#7074,1.);
#1820=VECTOR('',#7075,1.);
#1821=VECTOR('',#7078,1.);
#1822=VECTOR('',#7079,1.);
#1823=VECTOR('',#7080,1.);
#1824=VECTOR('',#7083,1.);
#1825=VECTOR('',#7084,1.);
#1826=VECTOR('',#7085,1.);
#1827=VECTOR('',#7088,1.);
#1828=VECTOR('',#7089,1.);
#1829=VECTOR('',#7100,0.235);
#1830=VECTOR('',#7105,0.25);
#1831=VECTOR('',#7110,0.2125);
#2131=CIRCLE('',#5559,0.22);
#2132=CIRCLE('',#5561,0.24505);
#2133=CIRCLE('',#5563,0.24505);
#2134=CIRCLE('',#5565,0.175);
#2495=VERTEX_POINT('',#9897);
#2496=VERTEX_POINT('',#9898);
#2497=VERTEX_POINT('',#9900);
#2498=VERTEX_POINT('',#9902);
#2499=VERTEX_POINT('',#9906);
#2500=VERTEX_POINT('',#9908);
#2501=VERTEX_POINT('',#9912);
#2502=VERTEX_POINT('',#9914);
#2503=VERTEX_POINT('',#9918);
#2504=VERTEX_POINT('',#9920);
#2505=VERTEX_POINT('',#9924);
#2506=VERTEX_POINT('',#9926);
#2507=VERTEX_POINT('',#9934);
#2508=VERTEX_POINT('',#9937);
#2509=VERTEX_POINT('',#9941);
#2510=VERTEX_POINT('',#9945);
#3038=EDGE_CURVE('',#2495,#2496,#1591,.T.);
#3039=EDGE_CURVE('',#2495,#2497,#1592,.T.);
#3040=EDGE_CURVE('',#2497,#2498,#1593,.T.);
#3041=EDGE_CURVE('',#2496,#2498,#1594,.T.);
#3042=EDGE_CURVE('',#2499,#2495,#1595,.T.);
#3043=EDGE_CURVE('',#2499,#2500,#1596,.T.);
#3044=EDGE_CURVE('',#2500,#2497,#1597,.T.);
#3045=EDGE_CURVE('',#2501,#2499,#1598,.T.);
#3046=EDGE_CURVE('',#2501,#2502,#1599,.T.);
#3047=EDGE_CURVE('',#2502,#2500,#1600,.T.);
#3048=EDGE_CURVE('',#2503,#2501,#1601,.T.);
#3049=EDGE_CURVE('',#2503,#2504,#1602,.T.);
#3050=EDGE_CURVE('',#2504,#2502,#1603,.T.);
#3051=EDGE_CURVE('',#2505,#2503,#1604,.T.);
#3052=EDGE_CURVE('',#2505,#2506,#1605,.T.);
#3053=EDGE_CURVE('',#2506,#2504,#1606,.T.);
#3054=EDGE_CURVE('',#2496,#2505,#1607,.T.);
#3055=EDGE_CURVE('',#2498,#2506,#1608,.T.);
#3056=EDGE_CURVE('',#2507,#2507,#2131,.T.);
#3057=EDGE_CURVE('',#2508,#2508,#2132,.T.);
#3058=EDGE_CURVE('',#2508,#2507,#1609,.T.);
#3059=EDGE_CURVE('',#2509,#2509,#2133,.F.);
#3060=EDGE_CURVE('',#2509,#2508,#1610,.T.);
#3061=EDGE_CURVE('',#2510,#2510,#2134,.T.);
#3062=EDGE_CURVE('',#2510,#2509,#1611,.T.);
#4117=ORIENTED_EDGE('',*,*,#3038,.F.);
#4118=ORIENTED_EDGE('',*,*,#3039,.T.);
#4119=ORIENTED_EDGE('',*,*,#3040,.T.);
#4120=ORIENTED_EDGE('',*,*,#3041,.F.);
#4121=ORIENTED_EDGE('',*,*,#3042,.F.);
#4122=ORIENTED_EDGE('',*,*,#3043,.T.);
#4123=ORIENTED_EDGE('',*,*,#3044,.T.);
#4124=ORIENTED_EDGE('',*,*,#3039,.F.);
#4125=ORIENTED_EDGE('',*,*,#3045,.F.);
#4126=ORIENTED_EDGE('',*,*,#3046,.T.);
#4127=ORIENTED_EDGE('',*,*,#3047,.T.);
#4128=ORIENTED_EDGE('',*,*,#3043,.F.);
#4129=ORIENTED_EDGE('',*,*,#3048,.F.);
#4130=ORIENTED_EDGE('',*,*,#3049,.T.);
#4131=ORIENTED_EDGE('',*,*,#3050,.T.);
#4132=ORIENTED_EDGE('',*,*,#3046,.F.);
#4133=ORIENTED_EDGE('',*,*,#3051,.F.);
#4134=ORIENTED_EDGE('',*,*,#3052,.T.);
#4135=ORIENTED_EDGE('',*,*,#3053,.T.);
#4136=ORIENTED_EDGE('',*,*,#3049,.F.);
#4137=ORIENTED_EDGE('',*,*,#3054,.F.);
#4138=ORIENTED_EDGE('',*,*,#3041,.T.);
#4139=ORIENTED_EDGE('',*,*,#3055,.T.);
#4140=ORIENTED_EDGE('',*,*,#3052,.F.);
#4141=ORIENTED_EDGE('',*,*,#3055,.F.);
#4142=ORIENTED_EDGE('',*,*,#3040,.F.);
#4143=ORIENTED_EDGE('',*,*,#3044,.F.);
#4144=ORIENTED_EDGE('',*,*,#3047,.F.);
#4145=ORIENTED_EDGE('',*,*,#3050,.F.);
#4146=ORIENTED_EDGE('',*,*,#3053,.F.);
#4147=ORIENTED_EDGE('',*,*,#3056,.F.);
#4148=ORIENTED_EDGE('',*,*,#3038,.T.);
#4149=ORIENTED_EDGE('',*,*,#3054,.T.);
#4150=ORIENTED_EDGE('',*,*,#3051,.T.);
#4151=ORIENTED_EDGE('',*,*,#3048,.T.);
#4152=ORIENTED_EDGE('',*,*,#3045,.T.);
#4153=ORIENTED_EDGE('',*,*,#3042,.T.);
#4154=ORIENTED_EDGE('',*,*,#3057,.F.);
#4155=ORIENTED_EDGE('',*,*,#3058,.T.);
#4156=ORIENTED_EDGE('',*,*,#3056,.T.);
#4157=ORIENTED_EDGE('',*,*,#3058,.F.);
#4158=ORIENTED_EDGE('',*,*,#3059,.F.);
#4159=ORIENTED_EDGE('',*,*,#3060,.T.);
#4160=ORIENTED_EDGE('',*,*,#3057,.T.);
#4161=ORIENTED_EDGE('',*,*,#3060,.F.);
#4162=ORIENTED_EDGE('',*,*,#3061,.F.);
#4163=ORIENTED_EDGE('',*,*,#3062,.T.);
#4164=ORIENTED_EDGE('',*,*,#3059,.T.);
#4165=ORIENTED_EDGE('',*,*,#3062,.F.);
#4166=ORIENTED_EDGE('',*,*,#3061,.T.);
#4284=CYLINDRICAL_SURFACE('',#5562,0.24505);
#4559=ADVANCED_FACE('',(#944),#661,.F.);
#4560=ADVANCED_FACE('',(#945),#662,.F.);
#4561=ADVANCED_FACE('',(#946),#663,.F.);
#4562=ADVANCED_FACE('',(#947),#664,.F.);
#4563=ADVANCED_FACE('',(#948),#665,.F.);
#4564=ADVANCED_FACE('',(#949),#666,.F.);
#4565=ADVANCED_FACE('',(#950),#667,.F.);
#4566=ADVANCED_FACE('',(#951,#536),#668,.T.);
#4567=ADVANCED_FACE('',(#952),#227,.T.);
#4568=ADVANCED_FACE('',(#953),#4284,.T.);
#4569=ADVANCED_FACE('',(#954),#228,.T.);
#4570=ADVANCED_FACE('',(#955),#669,.T.);
#4608=CLOSED_SHELL('',(#4559,#4560,#4561,#4562,#4563,#4564,#4565,#4566,
#4567,#4568,#4569,#4570));
#5550=AXIS2_PLACEMENT_3D('',#9895,#7058,#7059);
#5551=AXIS2_PLACEMENT_3D('',#9896,#7060,#7061);
#5552=AXIS2_PLACEMENT_3D('',#9905,#7066,#7067);
#5553=AXIS2_PLACEMENT_3D('',#9911,#7071,#7072);
#5554=AXIS2_PLACEMENT_3D('',#9917,#7076,#7077);
#5555=AXIS2_PLACEMENT_3D('',#9923,#7081,#7082);
#5556=AXIS2_PLACEMENT_3D('',#9929,#7086,#7087);
#5557=AXIS2_PLACEMENT_3D('',#9932,#7090,#7091);
#5558=AXIS2_PLACEMENT_3D('',#9933,#7092,#7093);
#5559=AXIS2_PLACEMENT_3D('',#9935,#7094,#7095);
#5560=AXIS2_PLACEMENT_3D('',#9936,#7096,#7097);
#5561=AXIS2_PLACEMENT_3D('',#9938,#7098,#7099);
#5562=AXIS2_PLACEMENT_3D('',#9940,#7101,#7102);
#5563=AXIS2_PLACEMENT_3D('',#9942,#7103,#7104);
#5564=AXIS2_PLACEMENT_3D('',#9944,#7106,#7107);
#5565=AXIS2_PLACEMENT_3D('',#9946,#7108,#7109);
#5566=AXIS2_PLACEMENT_3D('',#9948,#7111,#7112);
#7058=DIRECTION('axis',(0.,0.,1.));
#7059=DIRECTION('refdir',(1.,0.,0.));
#7060=DIRECTION('center_axis',(0.866025403784439,0.,-0.5));
#7061=DIRECTION('ref_axis',(0.5,0.,0.866025403784439));
#7062=DIRECTION('',(0.5,0.,0.866025403784439));
#7063=DIRECTION('',(0.,-1.,0.));
#7064=DIRECTION('',(0.5,0.,0.866025403784439));
#7065=DIRECTION('',(0.,-1.,0.));
#7066=DIRECTION('center_axis',(1.92296268638356E-16,0.,-1.));
#7067=DIRECTION('ref_axis',(1.,0.,1.92296268638356E-16));
#7068=DIRECTION('',(1.,0.,1.92296268638356E-16));
#7069=DIRECTION('',(0.,-1.,0.));
#7070=DIRECTION('',(1.,0.,1.92296268638356E-16));
#7071=DIRECTION('center_axis',(-0.866025403784439,0.,-0.5));
#7072=DIRECTION('ref_axis',(0.5,0.,-0.866025403784439));
#7073=DIRECTION('',(0.5,0.,-0.866025403784439));
#7074=DIRECTION('',(0.,-1.,0.));
#7075=DIRECTION('',(0.5,0.,-0.866025403784438));
#7076=DIRECTION('center_axis',(-0.866025403784439,0.,0.5));
#7077=DIRECTION('ref_axis',(-0.5,0.,-0.866025403784439));
#7078=DIRECTION('',(-0.5,0.,-0.866025403784439));
#7079=DIRECTION('',(0.,-1.,0.));
#7080=DIRECTION('',(-0.5,0.,-0.866025403784439));
#7081=DIRECTION('center_axis',(-1.92296268638356E-16,0.,1.));
#7082=DIRECTION('ref_axis',(-1.,0.,-1.92296268638356E-16));
#7083=DIRECTION('',(-1.,0.,-1.92296268638356E-16));
#7084=DIRECTION('',(0.,-1.,0.));
#7085=DIRECTION('',(-1.,0.,-1.92296268638356E-16));
#7086=DIRECTION('center_axis',(0.866025403784439,0.,0.5));
#7087=DIRECTION('ref_axis',(-0.5,0.,0.866025403784439));
#7088=DIRECTION('',(-0.5,0.,0.866025403784439));
#7089=DIRECTION('',(-0.5,0.,0.866025403784439));
#7090=DIRECTION('center_axis',(0.,-1.,0.));
#7091=DIRECTION('ref_axis',(0.,0.,-1.));
#7092=DIRECTION('center_axis',(0.,1.,0.));
#7093=DIRECTION('ref_axis',(0.,0.,1.));
#7094=DIRECTION('center_axis',(0.,-1.,0.));
#7095=DIRECTION('ref_axis',(1.,0.,0.));
#7096=DIRECTION('center_axis',(0.,-1.,0.));
#7097=DIRECTION('ref_axis',(1.,0.,0.));
#7098=DIRECTION('center_axis',(0.,-1.,0.));
#7099=DIRECTION('ref_axis',(1.,0.,0.));
#7100=DIRECTION('',(0.707106781186547,0.707106781186548,8.65956056235493E-17));
#7101=DIRECTION('center_axis',(0.,-1.,0.));
#7102=DIRECTION('ref_axis',(1.,0.,0.));
#7103=DIRECTION('center_axis',(0.,1.,0.));
#7104=DIRECTION('ref_axis',(1.,0.,0.));
#7105=DIRECTION('',(0.,1.,0.));
#7106=DIRECTION('center_axis',(0.,1.,0.));
#7107=DIRECTION('ref_axis',(1.,0.,0.));
#7108=DIRECTION('center_axis',(0.,-1.,0.));
#7109=DIRECTION('ref_axis',(1.,0.,0.));
#7110=DIRECTION('',(-0.707106781186547,0.707106781186548,-8.65956056235493E-17));
#7111=DIRECTION('center_axis',(0.,-1.,0.));
#7112=DIRECTION('ref_axis',(0.,0.,-1.));
#9895=CARTESIAN_POINT('',(0.,0.,0.));
#9896=CARTESIAN_POINT('Origin',(0.0721687836487032,0.,-0.125));
#9897=CARTESIAN_POINT('',(0.0721687836487032,0.,-0.125));
#9898=CARTESIAN_POINT('',(0.144337567297406,0.,0.));
#9899=CARTESIAN_POINT('',(0.117710979560879,0.,-0.0461186027918559));
#9900=CARTESIAN_POINT('',(0.0721687836487032,-0.25,-0.125));
#9901=CARTESIAN_POINT('',(0.0721687836487032,0.,-0.125));
#9902=CARTESIAN_POINT('',(0.144337567297406,-0.25,0.));
#9903=CARTESIAN_POINT('',(0.144337567297406,-0.25,0.));
#9904=CARTESIAN_POINT('',(0.144337567297406,0.,0.));
#9905=CARTESIAN_POINT('Origin',(-0.0721687836487032,0.,-0.125));
#9906=CARTESIAN_POINT('',(-0.0721687836487032,0.,-0.125));
#9907=CARTESIAN_POINT('',(0.0739156081756484,0.,-0.125));
#9908=CARTESIAN_POINT('',(-0.0721687836487032,-0.25,-0.125));
#9909=CARTESIAN_POINT('',(-0.0721687836487032,0.,-0.125));
#9910=CARTESIAN_POINT('',(0.0721687836487032,-0.25,-0.125));
#9911=CARTESIAN_POINT('Origin',(-0.144337567297406,0.,-4.16333634234434E-17));
#9912=CARTESIAN_POINT('',(-0.144337567297406,0.,-1.76762539787485E-17));
#9913=CARTESIAN_POINT('',(-0.0987953713852306,0.,-0.0788813972081442));
#9914=CARTESIAN_POINT('',(-0.144337567297406,-0.25,-2.77555756156289E-17));
#9915=CARTESIAN_POINT('',(-0.144337567297406,0.,-1.76762539787485E-17));
#9916=CARTESIAN_POINT('',(-0.0721687836487032,-0.25,-0.125));
#9917=CARTESIAN_POINT('Origin',(-0.0721687836487033,0.,0.125));
#9918=CARTESIAN_POINT('',(-0.0721687836487033,0.,0.125));
#9919=CARTESIAN_POINT('',(-0.0627109795608791,0.,0.141381397208144));
#9920=CARTESIAN_POINT('',(-0.0721687836487033,-0.25,0.125));
#9921=CARTESIAN_POINT('',(-0.0721687836487033,0.,0.125));
#9922=CARTESIAN_POINT('',(-0.144337567297406,-0.25,-1.76762539787485E-17));
#9923=CARTESIAN_POINT('Origin',(0.0721687836487032,0.,0.125));
#9924=CARTESIAN_POINT('',(0.0721687836487032,0.,0.125));
#9925=CARTESIAN_POINT('',(0.146084391824352,0.,0.125));
#9926=CARTESIAN_POINT('',(0.0721687836487032,-0.25,0.125));
#9927=CARTESIAN_POINT('',(0.0721687836487032,0.,0.125));
#9928=CARTESIAN_POINT('',(-0.0721687836487033,-0.25,0.125));
#9929=CARTESIAN_POINT('Origin',(0.144337567297406,0.,0.));
#9930=CARTESIAN_POINT('',(0.153795371385231,0.,-0.0163813972081441));
#9931=CARTESIAN_POINT('',(0.0721687836487032,-0.25,0.125));
#9932=CARTESIAN_POINT('Origin',(0.,-0.25,0.));
#9933=CARTESIAN_POINT('Origin',(0.22,0.,0.));
#9934=CARTESIAN_POINT('',(-0.22,-8.67361737988404E-18,-2.69422295812418E-17));
#9935=CARTESIAN_POINT('Origin',(0.,0.,0.));
#9936=CARTESIAN_POINT('Origin',(0.,-0.015,0.));
#9937=CARTESIAN_POINT('',(-0.24505,-0.02505,-3.00099698131059E-17));
#9938=CARTESIAN_POINT('Origin',(0.,-0.02505,0.));
#9939=CARTESIAN_POINT('',(-0.235,-0.015,-2.87791997799628E-17));
#9940=CARTESIAN_POINT('Origin',(0.,-0.3775,0.));
#9941=CARTESIAN_POINT('',(-0.24505,-0.72995,3.00099698131059E-17));
#9942=CARTESIAN_POINT('Origin',(0.,-0.72995,0.));
#9943=CARTESIAN_POINT('',(-0.24505,-0.3775,-3.00099698131059E-17));
#9944=CARTESIAN_POINT('Origin',(0.,-0.7625,0.));
#9945=CARTESIAN_POINT('',(-0.175,-0.8,-2.14313189850787E-17));
#9946=CARTESIAN_POINT('Origin',(0.,-0.8,0.));
#9947=CARTESIAN_POINT('',(-0.2125,-0.7625,-2.60237444818813E-17));
#9948=CARTESIAN_POINT('Origin',(0.,-0.8,0.));
#9986=UNCERTAINTY_MEASURE_WITH_UNIT(LENGTH_MEASURE(0.001),#10021,
'DISTANCE_ACCURACY_VALUE',
'Maximum model space distance between geometric entities at asserted c
onnectivities');
#9987=UNCERTAINTY_MEASURE_WITH_UNIT(LENGTH_MEASURE(0.001),#10021,
'DISTANCE_ACCURACY_VALUE',
'Maximum model space distance between geometric entities at asserted c
onnectivities');
#10019=(
GEOMETRIC_REPRESENTATION_CONTEXT(3)
GLOBAL_UNCERTAINTY_ASSIGNED_CONTEXT((#9986))
GLOBAL_UNIT_ASSIGNED_CONTEXT((#10021,#10023,#10024))
REPRESENTATION_CONTEXT('','3D')
);
#10020=(
GEOMETRIC_REPRESENTATION_CONTEXT(3)
GLOBAL_UNCERTAINTY_ASSIGNED_CONTEXT((#9987))
GLOBAL_UNIT_ASSIGNED_CONTEXT((#10021,#10023,#10024))
REPRESENTATION_CONTEXT('','3D')
);
#10021=(
LENGTH_UNIT()
NAMED_UNIT(*)
SI_UNIT(.CENTI.,.METRE.)
);
#10023=(
NAMED_UNIT(*)
PLANE_ANGLE_UNIT()
SI_UNIT($,.RADIAN.)
);
#10024=(
NAMED_UNIT(*)
SI_UNIT($,.STERADIAN.)
SOLID_ANGLE_UNIT()
);
#10056=SHAPE_DEFINITION_REPRESENTATION(#10128,#10166);
#10128=PRODUCT_DEFINITION_SHAPE('',$,#10199);
#10166=SHAPE_REPRESENTATION('',(#5550),#10019);
#10167=PRODUCT_DEFINITION_CONTEXT('part definition',#10265,'design');
#10199=PRODUCT_DEFINITION('Socket Set Screw - M5x8',
'Socket Set Screw - M5x8',#10231,#10167);
#10231=PRODUCT_DEFINITION_FORMATION('',$,#10298);
#10265=APPLICATION_CONTEXT(
'Core Data for Automotive Mechanical Design Process');
#10266=PRODUCT_CONTEXT('part definition',#10265,'mechanical');
#10298=PRODUCT('Socket Set Screw - M5x8','Socket Set Screw - M5x8',
'Socket Set Screw - M5x8',(#10266));
#10369=COLOUR_RGB('Black',0.12,0.14,0.17);
#10370=FILL_AREA_STYLE_COLOUR('',#10369);
#10371=FILL_AREA_STYLE('',(#10370));
#10372=SURFACE_STYLE_FILL_AREA(#10371);
#10373=SURFACE_SIDE_STYLE('',(#10372));
#10374=SURFACE_STYLE_USAGE(.BOTH.,#10373);
#10375=PRESENTATION_STYLE_ASSIGNMENT((#10374));
ENDSEC;
END-ISO-10303-21;
